ISO-10303-21;
HEADER;
FILE_DESCRIPTION (('STEP AP214'),
    '1' );
FILE_NAME ('circlip for shafts normal_din_Circlip DIN 471 - 10 x 1.step',
    '2026-10-27T17:01:19',
    ( '' ),
    ( '' ),
    'SwSTEP 2.0',
    'SolidWorks 2026',
    '' );
FILE_SCHEMA (( 'AUTOMOTIVE_DESIGN' ));
ENDSEC;

DATA;
#4=CIRCLE ( 'NONE', #4048, 4.799999999999999822 ) ;
#8=FACE_OUTER_BOUND ( 'NONE', #13413, .T. ) ;
#9=CIRCLE ( 'NONE', #4050, 0.7500000000000000000 ) ;
#42=CARTESIAN_POINT ( 'NONE',  ( 0.000000000000000000, 0.000000000000000000, 0.000000000000000000 ) ) ;
#68=ORIENTED_EDGE ( 'NONE', *, *, #2122, .F. ) ;
#81=ORIENTED_EDGE ( 'NONE', *, *, #14582, .T. ) ;
#94=DIRECTION ( 'NONE',  ( 1.000000000000000000, 0.000000000000000000, 0.000000000000000000 ) ) ;
#168=AXIS2_PLACEMENT_3D ( 'NONE', #10064, #3978, #5431 ) ;
#173=VERTEX_POINT ( 'NONE', #3127 ) ;
#191=DIRECTION ( 'NONE',  ( 1.000000000000000000, 0.000000000000000000, 0.000000000000000000 ) ) ;
#192=LINE ( 'NONE', #8454, #3753 ) ;
#246=AXIS2_PLACEMENT_3D ( 'NONE', #1497, #5996, #10494 ) ;
#279=CYLINDRICAL_SURFACE ( 'NONE', #8252, 4.799999999999999822 ) ;
#299=VERTEX_POINT ( 'NONE', #5768 ) ;
#328=CARTESIAN_POINT ( 'NONE',  ( -0.1481481481481481122, -4.797713218419819903, -1.000000000000000000 ) ) ;
#349=EDGE_CURVE ( 'NONE', #6917, #2433, #2048, .T. ) ;
#416=DIRECTION ( 'NONE',  ( 1.000000000000000000, 0.000000000000000000, 0.000000000000000000 ) ) ;
#447=CIRCLE ( 'NONE', #8706, 6.080745460913608902 ) ;
#451=ORIENTED_EDGE ( 'NONE', *, *, #8325, .F. ) ;
#456=AXIS2_PLACEMENT_3D ( 'NONE', #10677, #11553, #9278 ) ;
#458=DIRECTION ( 'NONE',  ( -0.000000000000000000, -0.000000000000000000, -1.000000000000000000 ) ) ;
#469=CIRCLE ( 'NONE', #11086, 8.099999999999999645 ) ;
#481=CARTESIAN_POINT ( 'NONE',  ( -5.686050877451574337, -5.768780236673276995, 0.000000000000000000 ) ) ;
#495=DIRECTION ( 'NONE',  ( 0.000000000000000000, 0.000000000000000000, 1.000000000000000000 ) ) ;
#501=AXIS2_PLACEMENT_3D ( 'NONE', #42, #3395, #11489 ) ;
#564=DIRECTION ( 'NONE',  ( 1.000000000000000000, 0.000000000000000000, 0.000000000000000000 ) ) ;
#566=DIRECTION ( 'NONE',  ( -0.000000000000000000, -0.000000000000000000, -1.000000000000000000 ) ) ;
#580=ORIENTED_EDGE ( 'NONE', *, *, #2612, .F. ) ;
#604=VERTEX_POINT ( 'NONE', #9966 ) ;
#611=VERTEX_POINT ( 'NONE', #3108 ) ;
#631=AXIS2_PLACEMENT_3D ( 'NONE', #3625, #2205, #3544 ) ;
#635=CYLINDRICAL_SURFACE ( 'NONE', #168, 0.7499999999999997780 ) ;
#695=CIRCLE ( 'NONE', #8953, 8.099999999999999645 ) ;
#818=VERTEX_POINT ( 'NONE', #9138 ) ;
#827=DIRECTION ( 'NONE',  ( 0.000000000000000000, 0.000000000000000000, 1.000000000000000000 ) ) ;
#836=DIRECTION ( 'NONE',  ( 1.000000000000000000, 0.000000000000000000, 0.000000000000000000 ) ) ;
#843=CARTESIAN_POINT ( 'NONE',  ( 4.078421086530217288, -3.990950201428958621, 0.000000000000000000 ) ) ;
#849=EDGE_CURVE ( 'NONE', #611, #4450, #13643, .T. ) ;
#869=FACE_OUTER_BOUND ( 'NONE', #12744, .T. ) ;
#896=AXIS2_PLACEMENT_3D ( 'NONE', #9531, #14093, #10700 ) ;
#907=VECTOR ( 'NONE', #4293, 999.9999999999998863 ) ;
#954=ORIENTED_EDGE ( 'NONE', *, *, #1532, .T. ) ;
#964=CIRCLE ( 'NONE', #8523, 0.7499999999999997780 ) ;
#977=CYLINDRICAL_SURFACE ( 'NONE', #1409, 6.080745460913608902 ) ;
#982=DIRECTION ( 'NONE',  ( -0.000000000000000000, -0.000000000000000000, -1.000000000000000000 ) ) ;
#1040=ADVANCED_FACE ( 'NONE', ( #8756 ), #635, .T. ) ;
#1093=SHAPE_DEFINITION_REPRESENTATION ( #10785, #5933 ) ;
#1128=FILL_AREA_STYLE_COLOUR ( '', #9466 ) ;
#1133=VECTOR ( 'NONE', #3132, 1000.000000000000000 ) ;
#1147=CARTESIAN_POINT ( 'NONE',  ( 0.000000000000000000, 0.000000000000000000, -1.000000000000000000 ) ) ;
#1175=DIRECTION ( 'NONE',  ( 1.000000000000000000, 0.000000000000000000, 0.000000000000000000 ) ) ;
#1193=EDGE_CURVE ( 'NONE', #818, #8680, #12496, .T. ) ;
#1215=ORIENTED_EDGE ( 'NONE', *, *, #9273, .T. ) ;
#1232=CARTESIAN_POINT ( 'NONE',  ( 1.250000000000000000, -6.429618962271402616, -1.000000000000000000 ) ) ;
#1245=AXIS2_PLACEMENT_3D ( 'NONE', #481, #1523, #8231 ) ;
#1281=EDGE_LOOP ( 'NONE', ( #4973, #2971, #14599, #4787, #9806, #8332, #7169, #8113, #6262, #12089, #4623, #4827, #11001, #11503, #12582, #10546 ) ) ;
#1288=SURFACE_STYLE_USAGE ( .BOTH. , #11399 ) ;
#1300=DIRECTION ( 'NONE',  ( 1.000000000000000000, 0.000000000000000000, 0.000000000000000000 ) ) ;
#1311=DIRECTION ( 'NONE',  ( 0.000000000000000000, 0.000000000000000000, 1.000000000000000000 ) ) ;
#1321=CARTESIAN_POINT ( 'NONE',  ( -2.000000000000000000, -6.429618962271402616, 0.000000000000000000 ) ) ;
#1322=CARTESIAN_POINT ( 'NONE',  ( 0.000000000000000000, 0.5192545390863916310, 0.000000000000000000 ) ) ;
#1348=AXIS2_PLACEMENT_3D ( 'NONE', #1232, #5735, #94 ) ;
#1380=CARTESIAN_POINT ( 'NONE',  ( -4.078421086530219064, -3.990950201428956845, 0.000000000000000000 ) ) ;
#1400=LINE ( 'NONE', #5761, #14573 ) ;
#1409=AXIS2_PLACEMENT_3D ( 'NONE', #13307, #4316, #5280 ) ;
#1446=DIRECTION ( 'NONE',  ( 0.000000000000000000, 0.000000000000000000, 1.000000000000000000 ) ) ;
#1497=CARTESIAN_POINT ( 'NONE',  ( -2.354826896168714434, -6.962563485461402024, -1.000000000000000000 ) ) ;
#1506=CARTESIAN_POINT ( 'NONE',  ( 5.686050877451574337, -5.768780236673276995, 0.000000000000000000 ) ) ;
#1523=DIRECTION ( 'NONE',  ( -0.000000000000000000, -0.000000000000000000, -1.000000000000000000 ) ) ;
#1532=EDGE_CURVE ( 'NONE', #6611, #818, #11041, .T. ) ;
#1543=ORIENTED_EDGE ( 'NONE', *, *, #8563, .F. ) ;
#1551=ORIENTED_EDGE ( 'NONE', *, *, #7851, .T. ) ;
#1579=DIRECTION ( 'NONE',  ( 1.000000000000000000, 0.000000000000000000, 0.000000000000000000 ) ) ;
#1580=CARTESIAN_POINT ( 'NONE',  ( 0.000000000000000000, 0.000000000000000000, -1.000000000000000000 ) ) ;
#1605=CARTESIAN_POINT ( 'NONE',  ( 5.686050877451574337, -5.768780236673276995, -1.000000000000000000 ) ) ;
#1683=CARTESIAN_POINT ( 'NONE',  ( 0.1481481481481481122, -4.797713218419819903, -1.000000000000000000 ) ) ;
#1709=CARTESIAN_POINT ( 'NONE',  ( 0.000000000000000000, 0.5192545390863916310, -1.000000000000000000 ) ) ;
#1812=DIRECTION ( 'NONE',  ( 1.000000000000000000, 0.000000000000000000, 0.000000000000000000 ) ) ;
#1815=ORIENTED_EDGE ( 'NONE', *, *, #12410, .T. ) ;
#1822=ORIENTED_EDGE ( 'NONE', *, *, #9164, .T. ) ;
#1837=ADVANCED_FACE ( 'NONE', ( #2596 ), #7235, .T. ) ;
#1838=CIRCLE ( 'NONE', #896, 6.080745460913608902 ) ;
#1842=LINE ( 'NONE', #9892, #907 ) ;
#1863=DIRECTION ( 'NONE',  ( 0.1305261922200524616, 0.9914448613738103822, -0.000000000000000000 ) ) ;
#1887=VECTOR ( 'NONE', #8738, 1000.000000000000000 ) ;
#1922=ORIENTED_EDGE ( 'NONE', *, *, #4212, .F. ) ;
#1950=CARTESIAN_POINT ( 'NONE',  ( 0.000000000000000000, 0.000000000000000000, 0.000000000000000000 ) ) ;
#1969=CARTESIAN_POINT ( 'NONE',  ( -4.799999999999999822, 5.878304635907294211E-16, 0.000000000000000000 ) ) ;
#2002=CARTESIAN_POINT ( 'NONE',  ( 0.000000000000000000, 0.000000000000000000, -1.000000000000000000 ) ) ;
#2014=ORIENTED_EDGE ( 'NONE', *, *, #849, .T. ) ;
#2048=CIRCLE ( 'NONE', #2765, 4.799999999999999822 ) ;
#2057=ORIENTED_EDGE ( 'NONE', *, *, #5293, .T. ) ;
#2058=ORIENTED_EDGE ( 'NONE', *, *, #10606, .T. ) ;
#2068=ADVANCED_FACE ( 'NONE', ( #14211 ), #13648, .F. ) ;
#2086=CYLINDRICAL_SURFACE ( 'NONE', #2110, 2.396904916527700102 ) ;
#2102=PLANE ( 'NONE',  #8269 ) ;
#2104=CARTESIAN_POINT ( 'NONE',  ( 1.250000000000000000, -6.429618962271402616, -1.000000000000000000 ) ) ;
#2110=AXIS2_PLACEMENT_3D ( 'NONE', #11105, #14501, #6894 ) ;
#2118=EDGE_CURVE ( 'NONE', #7440, #5405, #12913, .T. ) ;
#2122=EDGE_CURVE ( 'NONE', #173, #4517, #6550, .T. ) ;
#2127=EDGE_CURVE ( 'NONE', #3628, #7440, #8172, .T. ) ;
#2145=AXIS2_PLACEMENT_3D ( 'NONE', #6253, #9657, #13055 ) ;
#2152=DIRECTION ( 'NONE',  ( -0.000000000000000000, -0.000000000000000000, -1.000000000000000000 ) ) ;
#2153=CARTESIAN_POINT ( 'NONE',  ( 2.354826896168714434, -6.962563485461402024, -1.000000000000000000 ) ) ;
#2172=CARTESIAN_POINT ( 'NONE',  ( -0.1481481481481481122, -4.797713218419819903, -1.000000000000000000 ) ) ;
#2183=DIRECTION ( 'NONE',  ( 1.000000000000000000, 0.000000000000000000, 0.000000000000000000 ) ) ;
#2196=EDGE_LOOP ( 'NONE', ( #11046, #14061, #1815, #7159 ) ) ;
#2205=DIRECTION ( 'NONE',  ( 0.000000000000000000, 0.000000000000000000, 1.000000000000000000 ) ) ;
#2218=EDGE_CURVE ( 'NONE', #11861, #4517, #3980, .T. ) ;
#2231=EDGE_LOOP ( 'NONE', ( #10930, #68 ) ) ;
#2247=CARTESIAN_POINT ( 'NONE',  ( 0.1481481481481481122, -4.797713218419819903, -1.000000000000000000 ) ) ;
#2267=DIRECTION ( 'NONE',  ( 0.000000000000000000, 0.000000000000000000, 1.000000000000000000 ) ) ;
#2305=PRESENTATION_STYLE_ASSIGNMENT (( #1288 ) ) ;
#2433=VERTEX_POINT ( 'NONE', #2967 ) ;
#2514=VERTEX_POINT ( 'NONE', #2903 ) ;
#2564=CARTESIAN_POINT ( 'NONE',  ( 3.098410542199072637, -7.060458129626440815, -1.000000000000000000 ) ) ;
#2596=FACE_OUTER_BOUND ( 'NONE', #11255, .T. ) ;
#2612=EDGE_CURVE ( 'NONE', #13279, #11011, #1400, .T. ) ;
#2630=DIRECTION ( 'NONE',  ( 1.000000000000000000, 0.000000000000000000, 0.000000000000000000 ) ) ;
#2641=EDGE_LOOP ( 'NONE', ( #6484, #1215, #9398, #4878 ) ) ;
#2696=EDGE_CURVE ( 'NONE', #611, #11996, #1838, .T. ) ;
#2711=DIRECTION ( 'NONE',  ( 0.000000000000000000, 0.000000000000000000, 1.000000000000000000 ) ) ;
#2765=AXIS2_PLACEMENT_3D ( 'NONE', #3412, #3562, #9157 ) ;
#2774=ORIENTED_EDGE ( 'NONE', *, *, #349, .T. ) ;
#2788=DIRECTION ( 'NONE',  ( -0.000000000000000000, -0.000000000000000000, -1.000000000000000000 ) ) ;
#2836=EDGE_LOOP ( 'NONE', ( #8114, #3156, #8120, #2014 ) ) ;
#2850=CIRCLE ( 'NONE', #8504, 0.7499999999999997780 ) ;
#2869=( GEOMETRIC_REPRESENTATION_CONTEXT ( 3 ) GLOBAL_UNCERTAINTY_ASSIGNED_CONTEXT ( ( #8266 ) ) GLOBAL_UNIT_ASSIGNED_CONTEXT ( ( #13389, #5787, #10289 ) ) REPRESENTATION_CONTEXT ( 'NONE', 'WORKASPACE' ) );
#2873=DIRECTION ( 'NONE',  ( 1.000000000000000000, 0.000000000000000000, 0.000000000000000000 ) ) ;
#2889=EDGE_CURVE ( 'NONE', #6611, #10150, #13788, .T. ) ;
#2903=CARTESIAN_POINT ( 'NONE',  ( -2.595115354961444076, -7.673029147243174641, -1.000000000000000000 ) ) ;
#2919=ORIENTED_EDGE ( 'NONE', *, *, #5293, .F. ) ;
#2952=DIRECTION ( 'NONE',  ( 0.000000000000000000, 0.000000000000000000, 1.000000000000000000 ) ) ;
#2967=CARTESIAN_POINT ( 'NONE',  ( 0.1481481481481481122, -4.797713218419819903, 0.000000000000000000 ) ) ;
#2971=ORIENTED_EDGE ( 'NONE', *, *, #3175, .F. ) ;
#3011=VECTOR ( 'NONE', #7034, 1000.000000000000000 ) ;
#3033=CARTESIAN_POINT ( 'NONE',  ( 0.000000000000000000, 0.000000000000000000, -1.000000000000000000 ) ) ;
#3047=VERTEX_POINT ( 'NONE', #5083 ) ;
#3082=CIRCLE ( 'NONE', #5671, 0.7500000000000000000 ) ;
#3083=DIRECTION ( 'NONE',  ( 0.000000000000000000, 0.000000000000000000, 1.000000000000000000 ) ) ;
#3108=CARTESIAN_POINT ( 'NONE',  ( 4.078421086530217288, -3.990950201428958621, -1.000000000000000000 ) ) ;
#3127=CARTESIAN_POINT ( 'NONE',  ( 0.5000000000000000000, -6.429618962271402616, 0.000000000000000000 ) ) ;
#3132=DIRECTION ( 'NONE',  ( 0.000000000000000000, 0.000000000000000000, 1.000000000000000000 ) ) ;
#3156=ORIENTED_EDGE ( 'NONE', *, *, #3873, .F. ) ;
#3166=DIRECTION ( 'NONE',  ( 0.000000000000000000, 0.000000000000000000, 1.000000000000000000 ) ) ;
#3174=LINE ( 'NONE', #7677, #12028 ) ;
#3175=EDGE_CURVE ( 'NONE', #4781, #6611, #11235, .T. ) ;
#3187=CARTESIAN_POINT ( 'NONE',  ( -2.595115354961444076, -7.673029147243174641, -1.000000000000000000 ) ) ;
#3207=ORIENTED_EDGE ( 'NONE', *, *, #2889, .T. ) ;
#3218=ORIENTED_EDGE ( 'NONE', *, *, #10701, .T. ) ;
#3237=AXIS2_PLACEMENT_3D ( 'NONE', #4735, #9226, #416 ) ;
#3252=ORIENTED_EDGE ( 'NONE', *, *, #349, .F. ) ;
#3258=EDGE_LOOP ( 'NONE', ( #1543, #7786, #6655, #9287 ) ) ;
#3260=UNCERTAINTY_MEASURE_WITH_UNIT (LENGTH_MEASURE( 1.000000000000000082E-05 ), #9668, 'distance_accuracy_value', 'NONE');
#3267=ORIENTED_EDGE ( 'NONE', *, *, #13640, .F. ) ;
#3269=VECTOR ( 'NONE', #5844, 1000.000000000000000 ) ;
#3271=CARTESIAN_POINT ( 'NONE',  ( -0.1481481481481481122, -4.797713218419819903, -1.000000000000000000 ) ) ;
#3307=AXIS2_PLACEMENT_3D ( 'NONE', #6924, #1311, #1812 ) ;
#3372=CIRCLE ( 'NONE', #11838, 0.7499999999999997780 ) ;
#3395=DIRECTION ( 'NONE',  ( 0.000000000000000000, 0.000000000000000000, 1.000000000000000000 ) ) ;
#3404=ORIENTED_EDGE ( 'NONE', *, *, #9376, .T. ) ;
#3412=CARTESIAN_POINT ( 'NONE',  ( 0.000000000000000000, 0.000000000000000000, 0.000000000000000000 ) ) ;
#3424=VERTEX_POINT ( 'NONE', #6067 ) ;
#3437=EDGE_CURVE ( 'NONE', #8013, #604, #4977, .T. ) ;
#3440=ORIENTED_EDGE ( 'NONE', *, *, #11928, .T. ) ;
#3456=LINE ( 'NONE', #12448, #11804 ) ;
#3496=ORIENTED_EDGE ( 'NONE', *, *, #13714, .T. ) ;
#3508=VERTEX_POINT ( 'NONE', #9546 ) ;
#3515=CARTESIAN_POINT ( 'NONE',  ( -1.250000000000000000, -6.429618962271402616, -1.000000000000000000 ) ) ;
#3518=AXIS2_PLACEMENT_3D ( 'NONE', #3033, #5391, #6272 ) ;
#3522=DIRECTION ( 'NONE',  ( 0.000000000000000000, 0.000000000000000000, 1.000000000000000000 ) ) ;
#3541=CARTESIAN_POINT ( 'NONE',  ( 4.078421086530217288, -3.990950201428958621, -1.000000000000000000 ) ) ;
#3544=DIRECTION ( 'NONE',  ( 1.000000000000000000, 0.000000000000000000, 0.000000000000000000 ) ) ;
#3562=DIRECTION ( 'NONE',  ( -0.000000000000000000, -0.000000000000000000, -1.000000000000000000 ) ) ;
#3567=DIRECTION ( 'NONE',  ( 0.000000000000000000, 0.000000000000000000, 1.000000000000000000 ) ) ;
#3589=FILL_AREA_STYLE ('',( #1128 ) ) ;
#3591=ORIENTED_EDGE ( 'NONE', *, *, #7451, .T. ) ;
#3625=CARTESIAN_POINT ( 'NONE',  ( 0.000000000000000000, 0.000000000000000000, -1.000000000000000000 ) ) ;
#3628=VERTEX_POINT ( 'NONE', #10039 ) ;
#3685=CARTESIAN_POINT ( 'NONE',  ( 3.309651814758565180, -5.455921364805393026, -1.000000000000000000 ) ) ;
#3702=CARTESIAN_POINT ( 'NONE',  ( -0.2500000000000000000, -8.096141056083446585, 0.000000000000000000 ) ) ;
#3719=AXIS2_PLACEMENT_3D ( 'NONE', #1322, #10322, #191 ) ;
#3721=CIRCLE ( 'NONE', #14552, 2.396904916527699214 ) ;
#3730=ORIENTED_EDGE ( 'NONE', *, *, #7451, .F. ) ;
#3740=VERTEX_POINT ( 'NONE', #3702 ) ;
#3752=VECTOR ( 'NONE', #7985, 1000.000000000000114 ) ;
#3753=VECTOR ( 'NONE', #8043, 1000.000000000000114 ) ;
#3813=VECTOR ( 'NONE', #5439, 1000.000000000000000 ) ;
#3840=CARTESIAN_POINT ( 'NONE',  ( -5.686050877451574337, -5.768780236673276995, -1.000000000000000000 ) ) ;
#3847=VERTEX_POINT ( 'NONE', #14249 ) ;
#3873=EDGE_CURVE ( 'NONE', #3847, #6036, #5167, .T. ) ;
#3876=EDGE_CURVE ( 'NONE', #3508, #4822, #10702, .T. ) ;
#3901=ORIENTED_EDGE ( 'NONE', *, *, #5499, .F. ) ;
#3910=DIRECTION ( 'NONE',  ( 0.000000000000000000, 0.000000000000000000, 1.000000000000000000 ) ) ;
#3951=AXIS2_PLACEMENT_3D ( 'NONE', #1147, #3522, #6913 ) ;
#3978=DIRECTION ( 'NONE',  ( 0.000000000000000000, 0.000000000000000000, 1.000000000000000000 ) ) ;
#3980=LINE ( 'NONE', #12088, #10777 ) ;
#4028=CIRCLE ( 'NONE', #5907, 4.799999999999999822 ) ;
#4029=AXIS2_PLACEMENT_3D ( 'NONE', #9520, #8552, #13864 ) ;
#4048=AXIS2_PLACEMENT_3D ( 'NONE', #5748, #8033, #12536 ) ;
#4050=AXIS2_PLACEMENT_3D ( 'NONE', #4108, #827, #8594 ) ;
#4053=CARTESIAN_POINT ( 'NONE',  ( -0.5000000000000000000, -6.429618962271402616, -1.000000000000000000 ) ) ;
#4066=APPLICATION_CONTEXT ( 'automotive_design' ) ;
#4088=LINE ( 'NONE', #3187, #12251 ) ;
#4106=ORIENTED_EDGE ( 'NONE', *, *, #1193, .T. ) ;
#4108=CARTESIAN_POINT ( 'NONE',  ( 1.250000000000000000, -6.429618962271402616, -1.000000000000000000 ) ) ;
#4162=CARTESIAN_POINT ( 'NONE',  ( -0.5000000000000000000, -6.429618962271402616, -1.000000000000000000 ) ) ;
#4208=ADVANCED_BREP_SHAPE_REPRESENTATION ( '', ( #7105, #9440 ), #5461 ) ;
#4212=EDGE_CURVE ( 'NONE', #11364, #6968, #12008, .T. ) ;
#4213=VECTOR ( 'NONE', #1863, 999.9999999999998863 ) ;
#4237=VECTOR ( 'NONE', #13070, 1000.000000000000000 ) ;
#4238=CARTESIAN_POINT ( 'NONE',  ( 3.098410542199072637, -7.060458129626440815, -1.000000000000000000 ) ) ;
#4258=CARTESIAN_POINT ( 'NONE',  ( -1.250000000000000000, -6.429618962271402616, -1.000000000000000000 ) ) ;
#4268=ORIENTED_EDGE ( 'NONE', *, *, #11858, .F. ) ;
#4293=DIRECTION ( 'NONE',  ( 0.1305261922200524616, -0.9914448613738103822, 0.000000000000000000 ) ) ;
#4316=DIRECTION ( 'NONE',  ( 0.000000000000000000, 0.000000000000000000, 1.000000000000000000 ) ) ;
#4347=CARTESIAN_POINT ( 'NONE',  ( 0.000000000000000000, 0.000000000000000000, 0.000000000000000000 ) ) ;
#4406=CYLINDRICAL_SURFACE ( 'NONE', #9944, 6.080745460913608902 ) ;
#4407=DIRECTION ( 'NONE',  ( 0.000000000000000000, 0.000000000000000000, 1.000000000000000000 ) ) ;
#4435=CARTESIAN_POINT ( 'NONE',  ( 0.000000000000000000, 0.000000000000000000, -1.000000000000000000 ) ) ;
#4450=VERTEX_POINT ( 'NONE', #843 ) ;
#4451=DIRECTION ( 'NONE',  ( 1.000000000000000000, 0.000000000000000000, 0.000000000000000000 ) ) ;
#4480=AXIS2_PLACEMENT_3D ( 'NONE', #13675, #12570, #4451 ) ;
#4486=EDGE_CURVE ( 'NONE', #11996, #3628, #12017, .T. ) ;
#4506=CARTESIAN_POINT ( 'NONE',  ( -2.595115354961444076, -7.673029147243174641, 0.000000000000000000 ) ) ;
#4517=VERTEX_POINT ( 'NONE', #14370 ) ;
#4522=CIRCLE ( 'NONE', #8991, 2.396904916527700102 ) ;
#4544=ORIENTED_EDGE ( 'NONE', *, *, #6735, .T. ) ;
#4546=DIRECTION ( 'NONE',  ( 0.000000000000000000, 0.000000000000000000, 1.000000000000000000 ) ) ;
#4561=EDGE_CURVE ( 'NONE', #6968, #11364, #9683, .T. ) ;
#4608=ORIENTED_EDGE ( 'NONE', *, *, #12867, .T. ) ;
#4616=LINE ( 'NONE', #9103, #13671 ) ;
#4623=ORIENTED_EDGE ( 'NONE', *, *, #12410, .F. ) ;
#4631=LINE ( 'NONE', #5733, #8226 ) ;
#4651=CARTESIAN_POINT ( 'NONE',  ( -0.1481481481481481122, -4.797713218419819903, -1.000000000000000000 ) ) ;
#4654=ADVANCED_FACE ( 'NONE', ( #13619 ), #10453, .F. ) ;
#4673=CARTESIAN_POINT ( 'NONE',  ( -3.309651814758565180, -5.455921364805393026, -1.000000000000000000 ) ) ;
#4735=CARTESIAN_POINT ( 'NONE',  ( 1.250000000000000000, -6.429618962271402616, 0.000000000000000000 ) ) ;
#4744=DIRECTION ( 'NONE',  ( 0.000000000000000000, 0.000000000000000000, 1.000000000000000000 ) ) ;
#4781=VERTEX_POINT ( 'NONE', #13923 ) ;
#4787=ORIENTED_EDGE ( 'NONE', *, *, #9384, .F. ) ;
#4800=DIRECTION ( 'NONE',  ( 0.000000000000000000, 0.000000000000000000, 1.000000000000000000 ) ) ;
#4803=EDGE_CURVE ( 'NONE', #3508, #13279, #469, .T. ) ;
#4805=DIRECTION ( 'NONE',  ( 0.000000000000000000, 0.000000000000000000, 1.000000000000000000 ) ) ;
#4822=VERTEX_POINT ( 'NONE', #11755 ) ;
#4827=ORIENTED_EDGE ( 'NONE', *, *, #5484, .F. ) ;
#4868=EDGE_CURVE ( 'NONE', #10150, #8680, #4028, .T. ) ;
#4878=ORIENTED_EDGE ( 'NONE', *, *, #10443, .F. ) ;
#4896=ORIENTED_EDGE ( 'NONE', *, *, #13115, .T. ) ;
#4973=ORIENTED_EDGE ( 'NONE', *, *, #1532, .F. ) ;
#4977=LINE ( 'NONE', #13757, #3269 ) ;
#5052=CARTESIAN_POINT ( 'NONE',  ( 6.080745460913608902, 0.5192545390863916310, -1.000000000000000000 ) ) ;
#5083=CARTESIAN_POINT ( 'NONE',  ( 6.080745460913608902, 0.5192545390863916310, 0.000000000000000000 ) ) ;
#5167=LINE ( 'NONE', #8564, #10827 ) ;
#5232=VECTOR ( 'NONE', #7066, 999.9999999999998863 ) ;
#5235=CARTESIAN_POINT ( 'NONE',  ( 2.354826896168714434, -6.962563485461402024, -1.000000000000000000 ) ) ;
#5279=ORIENTED_EDGE ( 'NONE', *, *, #13115, .F. ) ;
#5280=DIRECTION ( 'NONE',  ( 1.000000000000000000, 0.000000000000000000, 0.000000000000000000 ) ) ;
#5293=EDGE_CURVE ( 'NONE', #4781, #3740, #3174, .T. ) ;
#5305=VERTEX_POINT ( 'NONE', #2564 ) ;
#5321=ORIENTED_EDGE ( 'NONE', *, *, #3876, .T. ) ;
#5342=CYLINDRICAL_SURFACE ( 'NONE', #12730, 0.7500000000000000000 ) ;
#5353=CARTESIAN_POINT ( 'NONE',  ( -2.000000000000000000, -6.429618962271402616, -1.000000000000000000 ) ) ;
#5391=DIRECTION ( 'NONE',  ( 0.000000000000000000, 0.000000000000000000, 1.000000000000000000 ) ) ;
#5405=VERTEX_POINT ( 'NONE', #1380 ) ;
#5431=DIRECTION ( 'NONE',  ( 1.000000000000000000, 0.000000000000000000, 0.000000000000000000 ) ) ;
#5439=DIRECTION ( 'NONE',  ( 0.000000000000000000, 0.000000000000000000, 1.000000000000000000 ) ) ;
#5454=ORIENTED_EDGE ( 'NONE', *, *, #5481, .F. ) ;
#5460=AXIS2_PLACEMENT_3D ( 'NONE', #10689, #14160, #564 ) ;
#5461=( GEOMETRIC_REPRESENTATION_CONTEXT ( 3 ) GLOBAL_UNCERTAINTY_ASSIGNED_CONTEXT ( ( #6051 ) ) GLOBAL_UNIT_ASSIGNED_CONTEXT ( ( #12580, #5640, #6898 ) ) REPRESENTATION_CONTEXT ( 'NONE', 'WORKASPACE' ) );
#5473=ADVANCED_FACE ( 'NONE', ( #8613 ), #8545, .T. ) ;
#5476=EDGE_LOOP ( 'NONE', ( #4268, #7297, #14511, #5723 ) ) ;
#5481=EDGE_CURVE ( 'NONE', #6009, #2433, #10613, .T. ) ;
#5484=EDGE_CURVE ( 'NONE', #13279, #5305, #964, .T. ) ;
#5499=EDGE_CURVE ( 'NONE', #3047, #7440, #12039, .T. ) ;
#5536=DIRECTION ( 'NONE',  ( 0.9995235871707960351, -0.03086419753086420970, 0.000000000000000000 ) ) ;
#5548=VERTEX_POINT ( 'NONE', #4053 ) ;
#5580=DIRECTION ( 'NONE',  ( 1.000000000000000000, 0.000000000000000000, 0.000000000000000000 ) ) ;
#5586=AXIS2_PLACEMENT_3D ( 'NONE', #1580, #9497, #7267 ) ;
#5611=DIRECTION ( 'NONE',  ( 1.000000000000000000, 0.000000000000000000, 0.000000000000000000 ) ) ;
#5615=VECTOR ( 'NONE', #4800, 1000.000000000000000 ) ;
#5626=DIRECTION ( 'NONE',  ( 0.000000000000000000, 0.000000000000000000, 1.000000000000000000 ) ) ;
#5640=( NAMED_UNIT ( * ) PLANE_ANGLE_UNIT ( ) SI_UNIT ( $, .RADIAN. ) );
#5644=EDGE_LOOP ( 'NONE', ( #14425, #2919, #13157, #3207 ) ) ;
#5671=AXIS2_PLACEMENT_3D ( 'NONE', #7966, #6653, #1175 ) ;
#5713=ORIENTED_EDGE ( 'NONE', *, *, #4212, .T. ) ;
#5715=ADVANCED_FACE ( 'NONE', ( #13331 ), #2102, .T. ) ;
#5723=ORIENTED_EDGE ( 'NONE', *, *, #2612, .T. ) ;
#5733=CARTESIAN_POINT ( 'NONE',  ( 0.5000000000000000000, -6.429618962271402616, -1.000000000000000000 ) ) ;
#5735=DIRECTION ( 'NONE',  ( 0.000000000000000000, 0.000000000000000000, 1.000000000000000000 ) ) ;
#5736=DIRECTION ( 'NONE',  ( 0.000000000000000000, 0.000000000000000000, 1.000000000000000000 ) ) ;
#5743=ORIENTED_EDGE ( 'NONE', *, *, #2122, .T. ) ;
#5748=CARTESIAN_POINT ( 'NONE',  ( 0.000000000000000000, 0.000000000000000000, 0.000000000000000000 ) ) ;
#5761=CARTESIAN_POINT ( 'NONE',  ( 2.595115354961440524, -7.673029147243177306, -1.000000000000000000 ) ) ;
#5768=CARTESIAN_POINT ( 'NONE',  ( -3.309651814758565180, -5.455921364805393026, 0.000000000000000000 ) ) ;
#5771=FACE_OUTER_BOUND ( 'NONE', #10668, .T. ) ;
#5787=( NAMED_UNIT ( * ) PLANE_ANGLE_UNIT ( ) SI_UNIT ( $, .RADIAN. ) );
#5844=DIRECTION ( 'NONE',  ( 0.000000000000000000, 0.000000000000000000, 1.000000000000000000 ) ) ;
#5873=PLANE ( 'NONE',  #3951 ) ;
#5907=AXIS2_PLACEMENT_3D ( 'NONE', #14280, #982, #9995 ) ;
#5933=SHAPE_REPRESENTATION ( 'circlip for shafts normal_din_Circlip DIN 471 - 10 x 1', ( #9440 ), #5461 ) ;
#5952=DIRECTION ( 'NONE',  ( 1.000000000000000000, 0.000000000000000000, 0.000000000000000000 ) ) ;
#5960=AXIS2_PLACEMENT_3D ( 'NONE', #9741, #3166, #13194 ) ;
#5977=ORIENTED_EDGE ( 'NONE', *, *, #4486, .T. ) ;
#5994=VERTEX_POINT ( 'NONE', #10811 ) ;
#5996=DIRECTION ( 'NONE',  ( 0.000000000000000000, 0.000000000000000000, 1.000000000000000000 ) ) ;
#6009=VERTEX_POINT ( 'NONE', #11686 ) ;
#6012=EDGE_CURVE ( 'NONE', #3424, #6009, #8166, .T. ) ;
#6036=VERTEX_POINT ( 'NONE', #8197 ) ;
#6038=DIRECTION ( 'NONE',  ( 0.000000000000000000, 0.000000000000000000, 1.000000000000000000 ) ) ;
#6042=ORIENTED_EDGE ( 'NONE', *, *, #8563, .T. ) ;
#6044=CARTESIAN_POINT ( 'NONE',  ( 0.000000000000000000, 0.000000000000000000, -1.000000000000000000 ) ) ;
#6051=UNCERTAINTY_MEASURE_WITH_UNIT (LENGTH_MEASURE( 1.000000000000000082E-05 ), #12580, 'distance_accuracy_value', 'NONE');
#6067=CARTESIAN_POINT ( 'NONE',  ( 4.799999999999999822, 0.000000000000000000, -1.000000000000000000 ) ) ;
#6081=ORIENTED_EDGE ( 'NONE', *, *, #6669, .T. ) ;
#6178=FACE_OUTER_BOUND ( 'NONE', #5476, .T. ) ;
#6192=ORIENTED_EDGE ( 'NONE', *, *, #13640, .T. ) ;
#6195=CARTESIAN_POINT ( 'NONE',  ( -0.5000000000000000000, -6.429618962271402616, 0.000000000000000000 ) ) ;
#6204=CIRCLE ( 'NONE', #5960, 8.099999999999999645 ) ;
#6207=CARTESIAN_POINT ( 'NONE',  ( -0.1481481481481481122, -4.797713218419819903, 0.000000000000000000 ) ) ;
#6211=ADVANCED_FACE ( 'NONE', ( #8904, #6979, #7882 ), #5873, .F. ) ;
#6221=LINE ( 'NONE', #5052, #13917 ) ;
#6253=CARTESIAN_POINT ( 'NONE',  ( -3.309651814758565180, -5.455921364805393026, -1.000000000000000000 ) ) ;
#6262=ORIENTED_EDGE ( 'NONE', *, *, #2696, .F. ) ;
#6272=DIRECTION ( 'NONE',  ( 1.000000000000000000, 0.000000000000000000, 0.000000000000000000 ) ) ;
#6274=ADVANCED_FACE ( 'NONE', ( #11344 ), #13711, .F. ) ;
#6292=CARTESIAN_POINT ( 'NONE',  ( 5.686050877451574337, -5.768780236673276995, -1.000000000000000000 ) ) ;
#6353=CYLINDRICAL_SURFACE ( 'NONE', #3518, 8.099999999999999645 ) ;
#6388=AXIS2_PLACEMENT_3D ( 'NONE', #1605, #2788, #2873 ) ;
#6417=DIRECTION ( 'NONE',  ( 1.000000000000000000, 0.000000000000000000, 0.000000000000000000 ) ) ;
#6419=ORIENTED_EDGE ( 'NONE', *, *, #9471, .F. ) ;
#6439=VERTEX_POINT ( 'NONE', #5353 ) ;
#6443=DIRECTION ( 'NONE',  ( 0.000000000000000000, 0.000000000000000000, 1.000000000000000000 ) ) ;
#6484=ORIENTED_EDGE ( 'NONE', *, *, #1193, .F. ) ;
#6520=LINE ( 'NONE', #13161, #13873 ) ;
#6550=CIRCLE ( 'NONE', #3237, 0.7500000000000000000 ) ;
#6576=EDGE_LOOP ( 'NONE', ( #3218, #11514 ) ) ;
#6611=VERTEX_POINT ( 'NONE', #2172 ) ;
#6625=DIRECTION ( 'NONE',  ( 0.03086419753086420623, -0.9995235871707959241, 0.000000000000000000 ) ) ;
#6626=ORIENTED_EDGE ( 'NONE', *, *, #8640, .T. ) ;
#6634=CIRCLE ( 'NONE', #246, 0.7499999999999997780 ) ;
#6653=DIRECTION ( 'NONE',  ( 0.000000000000000000, 0.000000000000000000, 1.000000000000000000 ) ) ;
#6655=ORIENTED_EDGE ( 'NONE', *, *, #9384, .T. ) ;
#6669=EDGE_CURVE ( 'NONE', #6036, #4450, #3721, .T. ) ;
#6670=DIRECTION ( 'NONE',  ( 1.000000000000000000, 0.000000000000000000, 0.000000000000000000 ) ) ;
#6714=ORIENTED_EDGE ( 'NONE', *, *, #6735, .F. ) ;
#6716=PLANE ( 'NONE',  #12946 ) ;
#6735=EDGE_CURVE ( 'NONE', #6439, #6968, #11677, .T. ) ;
#6740=ORIENTED_EDGE ( 'NONE', *, *, #2127, .T. ) ;
#6800=DIRECTION ( 'NONE',  ( 1.000000000000000000, 0.000000000000000000, 0.000000000000000000 ) ) ;
#6834=CARTESIAN_POINT ( 'NONE',  ( 0.000000000000000000, 0.5192545390863916310, -1.000000000000000000 ) ) ;
#6872=CIRCLE ( 'NONE', #9477, 6.080745460913608902 ) ;
#6882=ADVANCED_FACE ( 'NONE', ( #11897 ), #11830, .F. ) ;
#6894=DIRECTION ( 'NONE',  ( 1.000000000000000000, 0.000000000000000000, 0.000000000000000000 ) ) ;
#6895=CARTESIAN_POINT ( 'NONE',  ( -4.799999999999999822, 5.878304635907294211E-16, -1.000000000000000000 ) ) ;
#6898=( NAMED_UNIT ( * ) SI_UNIT ( $, .STERADIAN. ) SOLID_ANGLE_UNIT ( ) );
#6904=CIRCLE ( 'NONE', #1245, 2.396904916527700102 ) ;
#6913=DIRECTION ( 'NONE',  ( 1.000000000000000000, 0.000000000000000000, -0.000000000000000000 ) ) ;
#6917=VERTEX_POINT ( 'NONE', #11967 ) ;
#6924=CARTESIAN_POINT ( 'NONE',  ( -1.250000000000000000, -6.429618962271402616, 0.000000000000000000 ) ) ;
#6968=VERTEX_POINT ( 'NONE', #1321 ) ;
#6979=FACE_BOUND ( 'NONE', #6576, .T. ) ;
#6989=FACE_BOUND ( 'NONE', #2231, .T. ) ;
#7011=ORIENTED_EDGE ( 'NONE', *, *, #6012, .T. ) ;
#7034=DIRECTION ( 'NONE',  ( 0.000000000000000000, 0.000000000000000000, 1.000000000000000000 ) ) ;
#7039=AXIS2_PLACEMENT_3D ( 'NONE', #2153, #3567, #6800 ) ;
#7062=APPLICATION_CONTEXT ( 'automotive_design' ) ;
#7066=DIRECTION ( 'NONE',  ( 0.1305261922200524616, -0.9914448613738103822, 0.000000000000000000 ) ) ;
#7082=DIRECTION ( 'NONE',  ( 0.000000000000000000, 0.000000000000000000, 1.000000000000000000 ) ) ;
#7084=AXIS2_PLACEMENT_3D ( 'NONE', #3515, #1446, #5952 ) ;
#7105=MANIFOLD_SOLID_BREP ( 'Body', #14463 ) ;
#7117=DIRECTION ( 'NONE',  ( 1.000000000000000000, 0.000000000000000000, 0.000000000000000000 ) ) ;
#7136=CARTESIAN_POINT ( 'NONE',  ( 6.080745460913608902, 0.5192545390863916310, -1.000000000000000000 ) ) ;
#7159=ORIENTED_EDGE ( 'NONE', *, *, #3873, .T. ) ;
#7169=ORIENTED_EDGE ( 'NONE', *, *, #9164, .F. ) ;
#7235=CYLINDRICAL_SURFACE ( 'NONE', #11274, 6.080745460913608902 ) ;
#7267=DIRECTION ( 'NONE',  ( 1.000000000000000000, 0.000000000000000000, 0.000000000000000000 ) ) ;
#7297=ORIENTED_EDGE ( 'NONE', *, *, #3876, .F. ) ;
#7335=CIRCLE ( 'NONE', #13949, 0.7500000000000000000 ) ;
#7342=VECTOR ( 'NONE', #3083, 1000.000000000000000 ) ;
#7405=ORIENTED_EDGE ( 'NONE', *, *, #11928, .F. ) ;
#7440=VERTEX_POINT ( 'NONE', #12138 ) ;
#7451=EDGE_CURVE ( 'NONE', #5548, #6439, #12226, .T. ) ;
#7482=DIRECTION ( 'NONE',  ( 0.000000000000000000, 0.000000000000000000, 1.000000000000000000 ) ) ;
#7534=AXIS2_PLACEMENT_3D ( 'NONE', #4258, #13262, #10902 ) ;
#7576=CARTESIAN_POINT ( 'NONE',  ( -1.250000000000000000, -6.429618962271402616, -1.000000000000000000 ) ) ;
#7638=CARTESIAN_POINT ( 'NONE',  ( 1.250000000000000000, -6.429618962271402616, -1.000000000000000000 ) ) ;
#7677=CARTESIAN_POINT ( 'NONE',  ( -0.2500000000000000000, -8.096141056083446585, -1.000000000000000000 ) ) ;
#7695=ORIENTED_EDGE ( 'NONE', *, *, #2696, .T. ) ;
#7713=FACE_OUTER_BOUND ( 'NONE', #8044, .T. ) ;
#7740=ADVANCED_FACE ( 'NONE', ( #8813 ), #977, .T. ) ;
#7761=STYLED_ITEM('',(#14674),#7105);
#7786=ORIENTED_EDGE ( 'NONE', *, *, #3437, .F. ) ;
#7799=AXIS2_PLACEMENT_3D ( 'NONE', #8895, #12290, #2183 ) ;
#7844=PRODUCT_DEFINITION_FORMATION_WITH_SPECIFIED_SOURCE ( 'ANY', '', #14090, .NOT_KNOWN. ) ;
#7850=ADVANCED_FACE ( 'NONE', ( #11090 ), #5342, .F. ) ;
#7851=EDGE_CURVE ( 'NONE', #5305, #8880, #9841, .T. ) ;
#7882=FACE_OUTER_BOUND ( 'NONE', #1281, .T. ) ;
#7963=FACE_OUTER_BOUND ( 'NONE', #5644, .T. ) ;
#7966=CARTESIAN_POINT ( 'NONE',  ( -1.250000000000000000, -6.429618962271402616, -1.000000000000000000 ) ) ;
#7985=DIRECTION ( 'NONE',  ( 0.03086419753086420623, 0.9995235871707959241, -0.000000000000000000 ) ) ;
#8013=VERTEX_POINT ( 'NONE', #11597 ) ;
#8033=DIRECTION ( 'NONE',  ( -0.000000000000000000, -0.000000000000000000, -1.000000000000000000 ) ) ;
#8043=DIRECTION ( 'NONE',  ( 0.03086419753086420623, -0.9995235871707959241, 0.000000000000000000 ) ) ;
#8044=EDGE_LOOP ( 'NONE', ( #6714, #3730, #13627, #5713 ) ) ;
#8064=CARTESIAN_POINT ( 'NONE',  ( 0.000000000000000000, 0.5192545390863916310, -1.000000000000000000 ) ) ;
#8103=DIRECTION ( 'NONE',  ( 0.1305261922200524338, 0.9914448613738102711, 0.000000000000000000 ) ) ;
#8113=ORIENTED_EDGE ( 'NONE', *, *, #4486, .F. ) ;
#8114=ORIENTED_EDGE ( 'NONE', *, *, #6669, .F. ) ;
#8120=ORIENTED_EDGE ( 'NONE', *, *, #14580, .T. ) ;
#8144=DIRECTION ( 'NONE',  ( 0.000000000000000000, 0.000000000000000000, 1.000000000000000000 ) ) ;
#8164=LINE ( 'NONE', #8321, #5232 ) ;
#8166=CIRCLE ( 'NONE', #5586, 4.799999999999999822 ) ;
#8172=LINE ( 'NONE', #12683, #14082 ) ;
#8197=CARTESIAN_POINT ( 'NONE',  ( 3.309651814758564736, -5.455921364805393026, 0.000000000000000000 ) ) ;
#8226=VECTOR ( 'NONE', #4407, 1000.000000000000000 ) ;
#8228=CARTESIAN_POINT ( 'NONE',  ( 2.595115354961440524, -7.673029147243177306, 0.000000000000000000 ) ) ;
#8231=DIRECTION ( 'NONE',  ( 1.000000000000000000, 0.000000000000000000, 0.000000000000000000 ) ) ;
#8252=AXIS2_PLACEMENT_3D ( 'NONE', #6044, #4744, #12690 ) ;
#8266=UNCERTAINTY_MEASURE_WITH_UNIT (LENGTH_MEASURE( 1.000000000000000082E-05 ), #13389, 'distance_accuracy_value', 'NONE');
#8269=AXIS2_PLACEMENT_3D ( 'NONE', #2247, #11259, #6625 ) ;
#8278=AXIS2_PLACEMENT_3D ( 'NONE', #3685, #13726, #8103 ) ;
#8283=STYLED_ITEM ( 'NONE', ( #2305 ), #4208 ) ;
#8301=CIRCLE ( 'NONE', #11372, 0.7500000000000000000 ) ;
#8308=CYLINDRICAL_SURFACE ( 'NONE', #456, 8.099999999999999645 ) ;
#8315=ORIENTED_EDGE ( 'NONE', *, *, #849, .F. ) ;
#8321=CARTESIAN_POINT ( 'NONE',  ( -3.309651814758565180, -5.455921364805393026, 0.000000000000000000 ) ) ;
#8325=EDGE_CURVE ( 'NONE', #6439, #5548, #3082, .T. ) ;
#8332=ORIENTED_EDGE ( 'NONE', *, *, #10606, .F. ) ;
#8373=CARTESIAN_POINT ( 'NONE',  ( 0.000000000000000000, 0.000000000000000000, -1.000000000000000000 ) ) ;
#8418=DIRECTION ( 'NONE',  ( 0.000000000000000000, 0.000000000000000000, 1.000000000000000000 ) ) ;
#8454=CARTESIAN_POINT ( 'NONE',  ( 0.1481481481481481122, -4.797713218419819903, 0.000000000000000000 ) ) ;
#8504=AXIS2_PLACEMENT_3D ( 'NONE', #9369, #9450, #13956 ) ;
#8519=DIRECTION ( 'NONE',  ( 1.000000000000000000, 0.000000000000000000, 0.000000000000000000 ) ) ;
#8523=AXIS2_PLACEMENT_3D ( 'NONE', #5235, #495, #13117 ) ;
#8537=ORIENTED_EDGE ( 'NONE', *, *, #13714, .F. ) ;
#8545=PLANE ( 'NONE',  #2145 ) ;
#8548=ORIENTED_EDGE ( 'NONE', *, *, #10596, .F. ) ;
#8552=DIRECTION ( 'NONE',  ( 0.000000000000000000, 0.000000000000000000, 1.000000000000000000 ) ) ;
#8563=EDGE_CURVE ( 'NONE', #604, #14470, #2850, .T. ) ;
#8564=CARTESIAN_POINT ( 'NONE',  ( 3.309651814758564736, -5.455921364805393026, -1.000000000000000000 ) ) ;
#8581=CARTESIAN_POINT ( 'NONE',  ( 0.1481481481481481122, -4.797713218419819903, -1.000000000000000000 ) ) ;
#8589=LINE ( 'NONE', #4162, #1133 ) ;
#8594=DIRECTION ( 'NONE',  ( 1.000000000000000000, 0.000000000000000000, 0.000000000000000000 ) ) ;
#8613=FACE_OUTER_BOUND ( 'NONE', #11730, .T. ) ;
#8617=CARTESIAN_POINT ( 'NONE',  ( 2.000000000000000000, -6.429618962271402616, -1.000000000000000000 ) ) ;
#8640=EDGE_CURVE ( 'NONE', #5994, #5405, #12141, .T. ) ;
#8673=CYLINDRICAL_SURFACE ( 'NONE', #13280, 0.7500000000000000000 ) ;
#8680=VERTEX_POINT ( 'NONE', #1969 ) ;
#8690=DIRECTION ( 'NONE',  ( 1.000000000000000000, 0.000000000000000000, 0.000000000000000000 ) ) ;
#8702=( GEOMETRIC_REPRESENTATION_CONTEXT ( 3 ) GLOBAL_UNCERTAINTY_ASSIGNED_CONTEXT ( ( #3260 ) ) GLOBAL_UNIT_ASSIGNED_CONTEXT ( ( #9668, #14171, #14459 ) ) REPRESENTATION_CONTEXT ( 'NONE', 'WORKASPACE' ) );
#8706=AXIS2_PLACEMENT_3D ( 'NONE', #11262, #11411, #1300 ) ;
#8710=ORIENTED_EDGE ( 'NONE', *, *, #10516, .T. ) ;
#8738=DIRECTION ( 'NONE',  ( 0.000000000000000000, 0.000000000000000000, 1.000000000000000000 ) ) ;
#8756=FACE_OUTER_BOUND ( 'NONE', #3258, .T. ) ;
#8813=FACE_OUTER_BOUND ( 'NONE', #10460, .T. ) ;
#8880=VERTEX_POINT ( 'NONE', #10736 ) ;
#8890=CARTESIAN_POINT ( 'NONE',  ( -4.078421086530219064, -3.990950201428956845, -1.000000000000000000 ) ) ;
#8895=CARTESIAN_POINT ( 'NONE',  ( 0.000000000000000000, 0.5192545390863916310, -1.000000000000000000 ) ) ;
#8904=FACE_BOUND ( 'NONE', #12121, .T. ) ;
#8932=ORIENTED_EDGE ( 'NONE', *, *, #14023, .F. ) ;
#8953=AXIS2_PLACEMENT_3D ( 'NONE', #1950, #7482, #11974 ) ;
#8966=SHAPE_REPRESENTATION_RELATIONSHIP ( 'NONE' , 'NONE' ,  #5933, #4208 ) ;
#8991=AXIS2_PLACEMENT_3D ( 'NONE', #3840, #566, #10753 ) ;
#9051=CARTESIAN_POINT ( 'NONE',  ( -1.250000000000000000, -6.429618962271402616, 0.000000000000000000 ) ) ;
#9069=EDGE_CURVE ( 'NONE', #14470, #3740, #695, .T. ) ;
#9103=CARTESIAN_POINT ( 'NONE',  ( 4.799999999999999822, 0.000000000000000000, -1.000000000000000000 ) ) ;
#9113=EDGE_CURVE ( 'NONE', #10478, #11861, #9, .T. ) ;
#9134=FACE_OUTER_BOUND ( 'NONE', #2196, .T. ) ;
#9138=CARTESIAN_POINT ( 'NONE',  ( -4.799999999999999822, 5.878304635907294211E-16, -1.000000000000000000 ) ) ;
#9157=DIRECTION ( 'NONE',  ( 1.000000000000000000, 0.000000000000000000, 0.000000000000000000 ) ) ;
#9164=EDGE_CURVE ( 'NONE', #3628, #5994, #6872, .T. ) ;
#9218=PLANE ( 'NONE',  #8278 ) ;
#9226=DIRECTION ( 'NONE',  ( 0.000000000000000000, 0.000000000000000000, 1.000000000000000000 ) ) ;
#9262=DIRECTION ( 'NONE',  ( 0.000000000000000000, 0.000000000000000000, 1.000000000000000000 ) ) ;
#9263=CARTESIAN_POINT ( 'NONE',  ( -2.000000000000000000, -6.429618962271402616, -1.000000000000000000 ) ) ;
#9273=EDGE_CURVE ( 'NONE', #818, #3424, #9432, .T. ) ;
#9278=DIRECTION ( 'NONE',  ( 1.000000000000000000, 0.000000000000000000, 0.000000000000000000 ) ) ;
#9287=ORIENTED_EDGE ( 'NONE', *, *, #9471, .T. ) ;
#9294=DIRECTION ( 'NONE',  ( 0.03086419753086420623, 0.9995235871707959241, -0.000000000000000000 ) ) ;
#9369=CARTESIAN_POINT ( 'NONE',  ( -2.354826896168714434, -6.962563485461402024, 0.000000000000000000 ) ) ;
#9376=EDGE_CURVE ( 'NONE', #11996, #3047, #6221, .T. ) ;
#9384=EDGE_CURVE ( 'NONE', #8013, #2514, #6634, .T. ) ;
#9386=DIRECTION ( 'NONE',  ( 1.000000000000000000, 0.000000000000000000, 0.000000000000000000 ) ) ;
#9398=ORIENTED_EDGE ( 'NONE', *, *, #14023, .T. ) ;
#9432=CIRCLE ( 'NONE', #4480, 4.799999999999999822 ) ;
#9440=AXIS2_PLACEMENT_3D ( 'NONE', #4347, #14302, #6417 ) ;
#9450=DIRECTION ( 'NONE',  ( 0.000000000000000000, 0.000000000000000000, 1.000000000000000000 ) ) ;
#9461=PRODUCT_DEFINITION_CONTEXT ( 'detailed design', #4066, 'design' ) ;
#9466=COLOUR_RGB ( '',1.000000000000000000, 0.9490196078431372140, 0.9098039215686274384 ) ;
#9471=EDGE_CURVE ( 'NONE', #2514, #14470, #4088, .T. ) ;
#9477=AXIS2_PLACEMENT_3D ( 'NONE', #8064, #5626, #11387 ) ;
#9497=DIRECTION ( 'NONE',  ( -0.000000000000000000, -0.000000000000000000, -1.000000000000000000 ) ) ;
#9520=CARTESIAN_POINT ( 'NONE',  ( 0.000000000000000000, 0.000000000000000000, -1.000000000000000000 ) ) ;
#9522=EDGE_LOOP ( 'NONE', ( #3267, #10383, #11664, #11260 ) ) ;
#9531=CARTESIAN_POINT ( 'NONE',  ( 0.000000000000000000, 0.5192545390863916310, -1.000000000000000000 ) ) ;
#9546=CARTESIAN_POINT ( 'NONE',  ( 0.2499999999999966416, -8.096141056083448362, -1.000000000000000000 ) ) ;
#9550=ORIENTED_EDGE ( 'NONE', *, *, #12406, .F. ) ;
#9657=DIRECTION ( 'NONE',  ( -0.9914448613738102711, -0.1305261922200524338, 0.000000000000000000 ) ) ;
#9665=EDGE_LOOP ( 'NONE', ( #1922, #10018 ) ) ;
#9668=( LENGTH_UNIT ( ) NAMED_UNIT ( * ) SI_UNIT ( .MILLI., .METRE. ) );
#9683=CIRCLE ( 'NONE', #11783, 0.7500000000000000000 ) ;
#9727=ADVANCED_FACE ( 'NONE', ( #14543 ), #11293, .F. ) ;
#9741=CARTESIAN_POINT ( 'NONE',  ( 0.000000000000000000, 0.000000000000000000, 0.000000000000000000 ) ) ;
#9806=ORIENTED_EDGE ( 'NONE', *, *, #12867, .F. ) ;
#9813=ADVANCED_FACE ( 'NONE', ( #10415 ), #279, .F. ) ;
#9841=LINE ( 'NONE', #4238, #1887 ) ;
#9871=ORIENTED_EDGE ( 'NONE', *, *, #9113, .F. ) ;
#9872=AXIS2_PLACEMENT_3D ( 'NONE', #6292, #14340, #9913 ) ;
#9892=CARTESIAN_POINT ( 'NONE',  ( -3.309651814758565180, -5.455921364805393026, -1.000000000000000000 ) ) ;
#9913=DIRECTION ( 'NONE',  ( 1.000000000000000000, 0.000000000000000000, 0.000000000000000000 ) ) ;
#9918=ORIENTED_EDGE ( 'NONE', *, *, #9069, .F. ) ;
#9944=AXIS2_PLACEMENT_3D ( 'NONE', #6834, #11409, #5580 ) ;
#9966=CARTESIAN_POINT ( 'NONE',  ( -3.098410542199071749, -7.060458129626440815, 0.000000000000000000 ) ) ;
#9995=DIRECTION ( 'NONE',  ( 1.000000000000000000, 0.000000000000000000, 0.000000000000000000 ) ) ;
#10007=ORIENTED_EDGE ( 'NONE', *, *, #9069, .T. ) ;
#10018=ORIENTED_EDGE ( 'NONE', *, *, #4561, .F. ) ;
#10039=CARTESIAN_POINT ( 'NONE',  ( -6.080745460913608902, 0.5192545390863924082, -1.000000000000000000 ) ) ;
#10064=CARTESIAN_POINT ( 'NONE',  ( -2.354826896168714434, -6.962563485461402024, -1.000000000000000000 ) ) ;
#10111=ORIENTED_EDGE ( 'NONE', *, *, #4561, .T. ) ;
#10150=VERTEX_POINT ( 'NONE', #6207 ) ;
#10165=CARTESIAN_POINT ( 'NONE',  ( 2.354826896168714434, -6.962563485461402024, 0.000000000000000000 ) ) ;
#10289=( NAMED_UNIT ( * ) SI_UNIT ( $, .STERADIAN. ) SOLID_ANGLE_UNIT ( ) );
#10322=DIRECTION ( 'NONE',  ( 0.000000000000000000, 0.000000000000000000, 1.000000000000000000 ) ) ;
#10383=ORIENTED_EDGE ( 'NONE', *, *, #10701, .F. ) ;
#10415=FACE_OUTER_BOUND ( 'NONE', #2641, .T. ) ;
#10443=EDGE_CURVE ( 'NONE', #8680, #6917, #4, .T. ) ;
#10445=ADVANCED_FACE ( 'NONE', ( #12379, #6989, #13504 ), #14609, .T. ) ;
#10453=CYLINDRICAL_SURFACE ( 'NONE', #7084, 0.7500000000000000000 ) ;
#10460=EDGE_LOOP ( 'NONE', ( #5977, #6740, #3901, #11973 ) ) ;
#10465=ORIENTED_EDGE ( 'NONE', *, *, #2118, .F. ) ;
#10478=VERTEX_POINT ( 'NONE', #11422 ) ;
#10494=DIRECTION ( 'NONE',  ( 1.000000000000000000, 0.000000000000000000, 0.000000000000000000 ) ) ;
#10516=EDGE_CURVE ( 'NONE', #12649, #299, #3456, .T. ) ;
#10535=ADVANCED_FACE ( 'NONE', ( #9134 ), #9218, .T. ) ;
#10543=ORIENTED_EDGE ( 'NONE', *, *, #10516, .F. ) ;
#10546=ORIENTED_EDGE ( 'NONE', *, *, #9273, .F. ) ;
#10596=EDGE_CURVE ( 'NONE', #299, #604, #8164, .T. ) ;
#10606=EDGE_CURVE ( 'NONE', #5994, #12649, #4522, .T. ) ;
#10613=LINE ( 'NONE', #1683, #7342 ) ;
#10618=CIRCLE ( 'NONE', #6388, 2.396904916527699214 ) ;
#10668=EDGE_LOOP ( 'NONE', ( #7405, #580, #11872, #1551 ) ) ;
#10677=CARTESIAN_POINT ( 'NONE',  ( 0.000000000000000000, 0.000000000000000000, -1.000000000000000000 ) ) ;
#10689=CARTESIAN_POINT ( 'NONE',  ( 0.000000000000000000, 0.5192545390863916310, 0.000000000000000000 ) ) ;
#10692=CARTESIAN_POINT ( 'NONE',  ( 1.250000000000000000, -6.429618962271402616, 0.000000000000000000 ) ) ;
#10700=DIRECTION ( 'NONE',  ( 1.000000000000000000, 0.000000000000000000, 0.000000000000000000 ) ) ;
#10701=EDGE_CURVE ( 'NONE', #11861, #10478, #7335, .T. ) ;
#10702=LINE ( 'NONE', #11874, #4237 ) ;
#10736=CARTESIAN_POINT ( 'NONE',  ( 3.098410542199072637, -7.060458129626440815, 0.000000000000000000 ) ) ;
#10753=DIRECTION ( 'NONE',  ( 1.000000000000000000, 0.000000000000000000, 0.000000000000000000 ) ) ;
#10774=DIRECTION ( 'NONE',  ( 0.000000000000000000, 0.000000000000000000, 1.000000000000000000 ) ) ;
#10777=VECTOR ( 'NONE', #11926, 1000.000000000000000 ) ;
#10785=PRODUCT_DEFINITION_SHAPE ( 'NONE', 'NONE',  #13881 ) ;
#10811=CARTESIAN_POINT ( 'NONE',  ( -4.078421086530219064, -3.990950201428956845, -1.000000000000000000 ) ) ;
#10827=VECTOR ( 'NONE', #2952, 1000.000000000000000 ) ;
#10828=VECTOR ( 'NONE', #11957, 1000.000000000000114 ) ;
#10853=ADVANCED_FACE ( 'NONE', ( #13554 ), #4406, .T. ) ;
#10902=DIRECTION ( 'NONE',  ( 1.000000000000000000, 0.000000000000000000, 0.000000000000000000 ) ) ;
#10930=ORIENTED_EDGE ( 'NONE', *, *, #11602, .F. ) ;
#10975=DIRECTION ( 'NONE',  ( 0.000000000000000000, 0.000000000000000000, 1.000000000000000000 ) ) ;
#11001=ORIENTED_EDGE ( 'NONE', *, *, #4803, .F. ) ;
#11011=VERTEX_POINT ( 'NONE', #8228 ) ;
#11041=CIRCLE ( 'NONE', #12934, 4.799999999999999822 ) ;
#11046=ORIENTED_EDGE ( 'NONE', *, *, #12503, .F. ) ;
#11081=ORIENTED_EDGE ( 'NONE', *, *, #8325, .T. ) ;
#11086=AXIS2_PLACEMENT_3D ( 'NONE', #8373, #11685, #1579 ) ;
#11090=FACE_OUTER_BOUND ( 'NONE', #12785, .T. ) ;
#11105=CARTESIAN_POINT ( 'NONE',  ( -5.686050877451574337, -5.768780236673276995, -1.000000000000000000 ) ) ;
#11110=SURFACE_STYLE_FILL_AREA ( #3589 ) ;
#11166=ORIENTED_EDGE ( 'NONE', *, *, #11858, .T. ) ;
#11182=ORIENTED_EDGE ( 'NONE', *, *, #8640, .F. ) ;
#11235=LINE ( 'NONE', #3271, #3752 ) ;
#11255=EDGE_LOOP ( 'NONE', ( #13760, #1822, #6626, #10465 ) ) ;
#11259=DIRECTION ( 'NONE',  ( -0.9995235871707960351, -0.03086419753086420970, 0.000000000000000000 ) ) ;
#11260=ORIENTED_EDGE ( 'NONE', *, *, #11602, .T. ) ;
#11262=CARTESIAN_POINT ( 'NONE',  ( 0.000000000000000000, 0.5192545390863916310, 0.000000000000000000 ) ) ;
#11274=AXIS2_PLACEMENT_3D ( 'NONE', #1709, #10774, #9386 ) ;
#11286=DIRECTION ( 'NONE',  ( 0.03086419753086420623, 0.9995235871707959241, 0.000000000000000000 ) ) ;
#11293=CYLINDRICAL_SURFACE ( 'NONE', #12736, 4.799999999999999822 ) ;
#11343=MECHANICAL_DESIGN_GEOMETRIC_PRESENTATION_REPRESENTATION('',(#8283),#2869);
#11344=FACE_OUTER_BOUND ( 'NONE', #9522, .T. ) ;
#11364=VERTEX_POINT ( 'NONE', #6195 ) ;
#11372=AXIS2_PLACEMENT_3D ( 'NONE', #10692, #3910, #13060 ) ;
#11387=DIRECTION ( 'NONE',  ( 1.000000000000000000, 0.000000000000000000, 0.000000000000000000 ) ) ;
#11399=SURFACE_SIDE_STYLE ('',( #11110 ) ) ;
#11409=DIRECTION ( 'NONE',  ( 0.000000000000000000, 0.000000000000000000, 1.000000000000000000 ) ) ;
#11411=DIRECTION ( 'NONE',  ( 0.000000000000000000, 0.000000000000000000, 1.000000000000000000 ) ) ;
#11422=CARTESIAN_POINT ( 'NONE',  ( 0.5000000000000000000, -6.429618962271402616, -1.000000000000000000 ) ) ;
#11489=DIRECTION ( 'NONE',  ( 1.000000000000000000, 0.000000000000000000, -0.000000000000000000 ) ) ;
#11503=ORIENTED_EDGE ( 'NONE', *, *, #13339, .F. ) ;
#11514=ORIENTED_EDGE ( 'NONE', *, *, #9113, .T. ) ;
#11553=DIRECTION ( 'NONE',  ( 0.000000000000000000, 0.000000000000000000, 1.000000000000000000 ) ) ;
#11597=CARTESIAN_POINT ( 'NONE',  ( -3.098410542199071749, -7.060458129626440815, -1.000000000000000000 ) ) ;
#11602=EDGE_CURVE ( 'NONE', #4517, #173, #8301, .T. ) ;
#11664=ORIENTED_EDGE ( 'NONE', *, *, #2218, .T. ) ;
#11677=LINE ( 'NONE', #9263, #3011 ) ;
#11685=DIRECTION ( 'NONE',  ( 0.000000000000000000, 0.000000000000000000, 1.000000000000000000 ) ) ;
#11686=CARTESIAN_POINT ( 'NONE',  ( 0.1481481481481481122, -4.797713218419819903, -1.000000000000000000 ) ) ;
#11730=EDGE_LOOP ( 'NONE', ( #8548, #10543, #4608, #13664 ) ) ;
#11755=CARTESIAN_POINT ( 'NONE',  ( 0.2499999999999966416, -8.096141056083448362, 0.000000000000000000 ) ) ;
#11783=AXIS2_PLACEMENT_3D ( 'NONE', #9051, #8144, #2630 ) ;
#11784=CIRCLE ( 'NONE', #4029, 8.099999999999999645 ) ;
#11804=VECTOR ( 'NONE', #4805, 1000.000000000000000 ) ;
#11830=CYLINDRICAL_SURFACE ( 'NONE', #9872, 2.396904916527699214 ) ;
#11838=AXIS2_PLACEMENT_3D ( 'NONE', #10165, #5736, #12522 ) ;
#11858=EDGE_CURVE ( 'NONE', #4822, #11011, #6204, .T. ) ;
#11861=VERTEX_POINT ( 'NONE', #8617 ) ;
#11872=ORIENTED_EDGE ( 'NONE', *, *, #5484, .T. ) ;
#11874=CARTESIAN_POINT ( 'NONE',  ( 0.2499999999999966416, -8.096141056083448362, -1.000000000000000000 ) ) ;
#11891=CARTESIAN_POINT ( 'NONE',  ( 2.595115354961440524, -7.673029147243177306, -1.000000000000000000 ) ) ;
#11897=FACE_OUTER_BOUND ( 'NONE', #2836, .T. ) ;
#11926=DIRECTION ( 'NONE',  ( 0.000000000000000000, 0.000000000000000000, 1.000000000000000000 ) ) ;
#11928=EDGE_CURVE ( 'NONE', #11011, #8880, #3372, .T. ) ;
#11957=DIRECTION ( 'NONE',  ( 0.03086419753086420623, -0.9995235871707959241, 0.000000000000000000 ) ) ;
#11960=EDGE_CURVE ( 'NONE', #5405, #299, #6904, .T. ) ;
#11967=CARTESIAN_POINT ( 'NONE',  ( 4.799999999999999822, 0.000000000000000000, 0.000000000000000000 ) ) ;
#11968=LINE ( 'NONE', #12182, #4213 ) ;
#11973=ORIENTED_EDGE ( 'NONE', *, *, #9376, .F. ) ;
#11974=DIRECTION ( 'NONE',  ( 1.000000000000000000, 0.000000000000000000, 0.000000000000000000 ) ) ;
#11996=VERTEX_POINT ( 'NONE', #7136 ) ;
#12008=CIRCLE ( 'NONE', #3307, 0.7500000000000000000 ) ;
#12017=CIRCLE ( 'NONE', #7799, 6.080745460913608902 ) ;
#12028=VECTOR ( 'NONE', #2711, 1000.000000000000000 ) ;
#12039=CIRCLE ( 'NONE', #5460, 6.080745460913608902 ) ;
#12066=DIRECTION ( 'NONE',  ( 0.000000000000000000, 0.000000000000000000, 1.000000000000000000 ) ) ;
#12073=ORIENTED_EDGE ( 'NONE', *, *, #10443, .T. ) ;
#12088=CARTESIAN_POINT ( 'NONE',  ( 2.000000000000000000, -6.429618962271402616, -1.000000000000000000 ) ) ;
#12089=ORIENTED_EDGE ( 'NONE', *, *, #14580, .F. ) ;
#12121=EDGE_LOOP ( 'NONE', ( #3591, #11081 ) ) ;
#12137=EDGE_LOOP ( 'NONE', ( #5279, #5454, #14493, #5321 ) ) ;
#12138=CARTESIAN_POINT ( 'NONE',  ( -6.080745460913608902, 0.5192545390863924082, 0.000000000000000000 ) ) ;
#12141=LINE ( 'NONE', #8890, #3813 ) ;
#12143=EDGE_LOOP ( 'NONE', ( #954, #4106, #13538, #12546 ) ) ;
#12168=ADVANCED_FACE ( 'NONE', ( #7713 ), #8673, .F. ) ;
#12182=CARTESIAN_POINT ( 'NONE',  ( 3.309651814758565180, -5.455921364805393026, 0.000000000000000000 ) ) ;
#12202=ORIENTED_EDGE ( 'NONE', *, *, #12503, .T. ) ;
#12226=CIRCLE ( 'NONE', #7534, 0.7500000000000000000 ) ;
#12251=VECTOR ( 'NONE', #6443, 1000.000000000000000 ) ;
#12284=ORIENTED_EDGE ( 'NONE', *, *, #2118, .T. ) ;
#12290=DIRECTION ( 'NONE',  ( 0.000000000000000000, 0.000000000000000000, 1.000000000000000000 ) ) ;
#12299=ORIENTED_EDGE ( 'NONE', *, *, #2218, .F. ) ;
#12316=ORIENTED_EDGE ( 'NONE', *, *, #10596, .T. ) ;
#12326=DIRECTION ( 'NONE',  ( 0.000000000000000000, 0.000000000000000000, 1.000000000000000000 ) ) ;
#12379=FACE_BOUND ( 'NONE', #9665, .T. ) ;
#12406=EDGE_CURVE ( 'NONE', #5548, #11364, #8589, .T. ) ;
#12410=EDGE_CURVE ( 'NONE', #5305, #3847, #6520, .T. ) ;
#12448=CARTESIAN_POINT ( 'NONE',  ( -3.309651814758565180, -5.455921364805393026, -1.000000000000000000 ) ) ;
#12491=VECTOR ( 'NONE', #9294, 1000.000000000000114 ) ;
#12496=LINE ( 'NONE', #6895, #13859 ) ;
#12503=EDGE_CURVE ( 'NONE', #8880, #6036, #11968, .T. ) ;
#12522=DIRECTION ( 'NONE',  ( -1.000000000000000000, 0.000000000000000000, 0.000000000000000000 ) ) ;
#12536=DIRECTION ( 'NONE',  ( 1.000000000000000000, 0.000000000000000000, 0.000000000000000000 ) ) ;
#12546=ORIENTED_EDGE ( 'NONE', *, *, #2889, .F. ) ;
#12567=ADVANCED_FACE ( 'NONE', ( #5771 ), #13454, .T. ) ;
#12570=DIRECTION ( 'NONE',  ( -0.000000000000000000, -0.000000000000000000, -1.000000000000000000 ) ) ;
#12580=( LENGTH_UNIT ( ) NAMED_UNIT ( * ) SI_UNIT ( .MILLI., .METRE. ) );
#12582=ORIENTED_EDGE ( 'NONE', *, *, #6012, .F. ) ;
#12609=CARTESIAN_POINT ( 'NONE',  ( -0.1481481481481481122, -4.797713218419819903, 0.000000000000000000 ) ) ;
#12649=VERTEX_POINT ( 'NONE', #4673 ) ;
#12683=CARTESIAN_POINT ( 'NONE',  ( -6.080745460913608902, 0.5192545390863924082, -1.000000000000000000 ) ) ;
#12690=DIRECTION ( 'NONE',  ( 1.000000000000000000, 0.000000000000000000, 0.000000000000000000 ) ) ;
#12730=AXIS2_PLACEMENT_3D ( 'NONE', #7638, #13029, #8519 ) ;
#12736=AXIS2_PLACEMENT_3D ( 'NONE', #4435, #12326, #5611 ) ;
#12744=EDGE_LOOP ( 'NONE', ( #9918, #6419, #81, #2057 ) ) ;
#12778=EDGE_LOOP ( 'NONE', ( #451, #4544, #10111, #9550 ) ) ;
#12785=EDGE_LOOP ( 'NONE', ( #9871, #6192, #5743, #12299 ) ) ;
#12867=EDGE_CURVE ( 'NONE', #12649, #8013, #1842, .T. ) ;
#12873=ADVANCED_FACE ( 'NONE', ( #869 ), #6353, .T. ) ;
#12913=CIRCLE ( 'NONE', #3719, 6.080745460913608902 ) ;
#12934=AXIS2_PLACEMENT_3D ( 'NONE', #2002, #2152, #6670 ) ;
#12946=AXIS2_PLACEMENT_3D ( 'NONE', #4651, #5536, #11286 ) ;
#13012=ADVANCED_FACE ( 'NONE', ( #7963 ), #6716, .T. ) ;
#13029=DIRECTION ( 'NONE',  ( 0.000000000000000000, 0.000000000000000000, 1.000000000000000000 ) ) ;
#13055=DIRECTION ( 'NONE',  ( 0.1305261922200524338, -0.9914448613738102711, 0.000000000000000000 ) ) ;
#13060=DIRECTION ( 'NONE',  ( 1.000000000000000000, 0.000000000000000000, 0.000000000000000000 ) ) ;
#13067=ORIENTED_EDGE ( 'NONE', *, *, #4868, .T. ) ;
#13070=DIRECTION ( 'NONE',  ( 0.000000000000000000, 0.000000000000000000, 1.000000000000000000 ) ) ;
#13095=DIRECTION ( 'NONE',  ( 0.1305261922200524616, 0.9914448613738103822, -0.000000000000000000 ) ) ;
#13115=EDGE_CURVE ( 'NONE', #2433, #4822, #192, .T. ) ;
#13117=DIRECTION ( 'NONE',  ( -1.000000000000000000, 0.000000000000000000, 0.000000000000000000 ) ) ;
#13157=ORIENTED_EDGE ( 'NONE', *, *, #3175, .T. ) ;
#13161=CARTESIAN_POINT ( 'NONE',  ( 3.309651814758565180, -5.455921364805393026, -1.000000000000000000 ) ) ;
#13185=MECHANICAL_DESIGN_GEOMETRIC_PRESENTATION_REPRESENTATION('',(#7761),#8702);
#13194=DIRECTION ( 'NONE',  ( 1.000000000000000000, 0.000000000000000000, 0.000000000000000000 ) ) ;
#13197=EDGE_LOOP ( 'NONE', ( #13067, #12073, #2774, #4896, #11166, #3440, #12202, #6081, #3496, #13621, #12284, #14492, #12316, #6042, #10007, #13494 ) ) ;
#13262=DIRECTION ( 'NONE',  ( 0.000000000000000000, 0.000000000000000000, 1.000000000000000000 ) ) ;
#13279=VERTEX_POINT ( 'NONE', #11891 ) ;
#13280=AXIS2_PLACEMENT_3D ( 'NONE', #7576, #12066, #836 ) ;
#13307=CARTESIAN_POINT ( 'NONE',  ( 0.000000000000000000, 0.5192545390863916310, -1.000000000000000000 ) ) ;
#13331=FACE_OUTER_BOUND ( 'NONE', #12137, .T. ) ;
#13339=EDGE_CURVE ( 'NONE', #6009, #3508, #14197, .T. ) ;
#13375=ORIENTED_EDGE ( 'NONE', *, *, #5481, .T. ) ;
#13389=( LENGTH_UNIT ( ) NAMED_UNIT ( * ) SI_UNIT ( .MILLI., .METRE. ) );
#13413=EDGE_LOOP ( 'NONE', ( #14027, #11182, #2058, #8710 ) ) ;
#13454=CYLINDRICAL_SURFACE ( 'NONE', #7039, 0.7499999999999997780 ) ;
#13494=ORIENTED_EDGE ( 'NONE', *, *, #14432, .T. ) ;
#13504=FACE_OUTER_BOUND ( 'NONE', #13197, .T. ) ;
#13508=LINE ( 'NONE', #12609, #12491 ) ;
#13538=ORIENTED_EDGE ( 'NONE', *, *, #4868, .F. ) ;
#13554=FACE_OUTER_BOUND ( 'NONE', #14578, .T. ) ;
#13619=FACE_OUTER_BOUND ( 'NONE', #12778, .T. ) ;
#13621=ORIENTED_EDGE ( 'NONE', *, *, #5499, .T. ) ;
#13627=ORIENTED_EDGE ( 'NONE', *, *, #12406, .T. ) ;
#13640=EDGE_CURVE ( 'NONE', #10478, #173, #4631, .T. ) ;
#13643=LINE ( 'NONE', #3541, #14565 ) ;
#13648=CYLINDRICAL_SURFACE ( 'NONE', #631, 4.799999999999999822 ) ;
#13664=ORIENTED_EDGE ( 'NONE', *, *, #3437, .T. ) ;
#13671=VECTOR ( 'NONE', #4546, 1000.000000000000000 ) ;
#13675=CARTESIAN_POINT ( 'NONE',  ( 0.000000000000000000, 0.000000000000000000, -1.000000000000000000 ) ) ;
#13711=CYLINDRICAL_SURFACE ( 'NONE', #1348, 0.7500000000000000000 ) ;
#13714=EDGE_CURVE ( 'NONE', #4450, #3047, #447, .T. ) ;
#13726=DIRECTION ( 'NONE',  ( 0.9914448613738102711, -0.1305261922200524338, 0.000000000000000000 ) ) ;
#13757=CARTESIAN_POINT ( 'NONE',  ( -3.098410542199071749, -7.060458129626440815, -1.000000000000000000 ) ) ;
#13760=ORIENTED_EDGE ( 'NONE', *, *, #2127, .F. ) ;
#13776=ADVANCED_FACE ( 'NONE', ( #6178 ), #8308, .T. ) ;
#13788=LINE ( 'NONE', #328, #5615 ) ;
#13859=VECTOR ( 'NONE', #9262, 1000.000000000000000 ) ;
#13864=DIRECTION ( 'NONE',  ( 1.000000000000000000, 0.000000000000000000, 0.000000000000000000 ) ) ;
#13873=VECTOR ( 'NONE', #13095, 999.9999999999998863 ) ;
#13881=PRODUCT_DEFINITION ( 'UNKNOWN', '', #7844, #9461 ) ;
#13917=VECTOR ( 'NONE', #8418, 1000.000000000000000 ) ;
#13923=CARTESIAN_POINT ( 'NONE',  ( -0.2500000000000000000, -8.096141056083446585, -1.000000000000000000 ) ) ;
#13949=AXIS2_PLACEMENT_3D ( 'NONE', #2104, #10975, #8690 ) ;
#13956=DIRECTION ( 'NONE',  ( 1.000000000000000000, 0.000000000000000000, 0.000000000000000000 ) ) ;
#13960=ADVANCED_FACE ( 'NONE', ( #8 ), #2086, .F. ) ;
#14023=EDGE_CURVE ( 'NONE', #3424, #6917, #4616, .T. ) ;
#14027=ORIENTED_EDGE ( 'NONE', *, *, #11960, .F. ) ;
#14038=EDGE_LOOP ( 'NONE', ( #8932, #7011, #13375, #3252 ) ) ;
#14061=ORIENTED_EDGE ( 'NONE', *, *, #7851, .F. ) ;
#14082=VECTOR ( 'NONE', #6038, 1000.000000000000000 ) ;
#14090=PRODUCT ( 'circlip for shafts normal_din_Circlip DIN 471 - 10 x 1', 'circlip for shafts normal_din_Circlip DIN 471 - 10 x 1', '', ( #14474 ) ) ;
#14093=DIRECTION ( 'NONE',  ( 0.000000000000000000, 0.000000000000000000, 1.000000000000000000 ) ) ;
#14160=DIRECTION ( 'NONE',  ( 0.000000000000000000, 0.000000000000000000, 1.000000000000000000 ) ) ;
#14171=( NAMED_UNIT ( * ) PLANE_ANGLE_UNIT ( ) SI_UNIT ( $, .RADIAN. ) );
#14197=LINE ( 'NONE', #8581, #10828 ) ;
#14211=FACE_OUTER_BOUND ( 'NONE', #12143, .T. ) ;
#14249=CARTESIAN_POINT ( 'NONE',  ( 3.309651814758564736, -5.455921364805393026, -1.000000000000000000 ) ) ;
#14280=CARTESIAN_POINT ( 'NONE',  ( 0.000000000000000000, 0.000000000000000000, 0.000000000000000000 ) ) ;
#14302=DIRECTION ( 'NONE',  ( 0.000000000000000000, 0.000000000000000000, 1.000000000000000000 ) ) ;
#14340=DIRECTION ( 'NONE',  ( 0.000000000000000000, 0.000000000000000000, 1.000000000000000000 ) ) ;
#14370=CARTESIAN_POINT ( 'NONE',  ( 2.000000000000000000, -6.429618962271402616, 0.000000000000000000 ) ) ;
#14425=ORIENTED_EDGE ( 'NONE', *, *, #14432, .F. ) ;
#14432=EDGE_CURVE ( 'NONE', #3740, #10150, #13508, .T. ) ;
#14459=( NAMED_UNIT ( * ) SI_UNIT ( $, .STERADIAN. ) SOLID_ANGLE_UNIT ( ) );
#14463=CLOSED_SHELL ( 'NONE', ( #4654, #7850, #7740, #10853, #2068, #9813, #9727, #13012, #12873, #1040, #5473, #13960, #1837, #6882, #10535, #12567, #13776, #5715, #6211, #10445, #6274, #12168 ) ) ;
#14470=VERTEX_POINT ( 'NONE', #4506 ) ;
#14474=PRODUCT_CONTEXT ( 'NONE', #7062, 'mechanical' ) ;
#14492=ORIENTED_EDGE ( 'NONE', *, *, #11960, .T. ) ;
#14493=ORIENTED_EDGE ( 'NONE', *, *, #13339, .T. ) ;
#14501=DIRECTION ( 'NONE',  ( 0.000000000000000000, 0.000000000000000000, 1.000000000000000000 ) ) ;
#14511=ORIENTED_EDGE ( 'NONE', *, *, #4803, .T. ) ;
#14543=FACE_OUTER_BOUND ( 'NONE', #14038, .T. ) ;
#14552=AXIS2_PLACEMENT_3D ( 'NONE', #1506, #458, #7117 ) ;
#14565=VECTOR ( 'NONE', #2267, 1000.000000000000000 ) ;
#14573=VECTOR ( 'NONE', #7082, 1000.000000000000000 ) ;
#14578=EDGE_LOOP ( 'NONE', ( #7695, #3404, #8537, #8315 ) ) ;
#14580=EDGE_CURVE ( 'NONE', #3847, #611, #10618, .T. ) ;
#14582=EDGE_CURVE ( 'NONE', #2514, #4781, #11784, .T. ) ;
#14599=ORIENTED_EDGE ( 'NONE', *, *, #14582, .F. ) ;
#14609=PLANE ( 'NONE',  #501 ) ;
#14668=COLOUR_RGB('Grey',0.48,0.52,0.57);
#14669=FILL_AREA_STYLE_COLOUR('',#14668);
#14670=FILL_AREA_STYLE('',(#14669));
#14671=SURFACE_STYLE_FILL_AREA(#14670);
#14672=SURFACE_SIDE_STYLE('',(#14671));
#14673=SURFACE_STYLE_USAGE(.BOTH.,#14672);
#14674=PRESENTATION_STYLE_ASSIGNMENT((#14673));
ENDSEC;
END-ISO-10303-21;
